ISO-10303-21;
HEADER;
FILE_DESCRIPTION (('STEP AP203'),
    '1' );
FILE_NAME ('Washer_Predeterminado.step',
    '2026-10-08T11:28:20',
    ( '' ),
    ( '' ),
    'SwSTEP 2.0',
    'SolidWorks 2024',
    '' );
FILE_SCHEMA (( 'AUTOMOTIVE_DESIGN' ));
ENDSEC;

DATA;
#126=SHAPE_DEFINITION_REPRESENTATION ( #5707, #10790 ) ;
#250=ORIENTED_EDGE ( 'NONE', *, *, #1589, .T. ) ;
#278=AXIS2_PLACEMENT_3D ( 'NONE', #4367, #11396, #11245 ) ;
#365=EDGE_CURVE ( 'NONE', #14267, #13371, #3381, .T. ) ;
#382=CARTESIAN_POINT ( 'NONE',  ( 0.000000000000000000, 0.000000000000000000, 0.000000000000000000 ) ) ;
#501=CARTESIAN_POINT ( 'NONE',  ( 7.347880794884122694E-16, 1.000000000000000000, 6.000000000000002665 ) ) ;
#531=EDGE_LOOP ( 'NONE', ( #11710, #5014, #10562, #10714 ) ) ;
#605=CIRCLE ( 'NONE', #6521, 6.000000000000002665 ) ;
#856=CYLINDRICAL_SURFACE ( 'NONE', #10635, 3.500000000000000000 ) ;
#872=DIRECTION ( 'NONE',  ( -0.000000000000000000, -1.000000000000000000, -0.000000000000000000 ) ) ;
#883=DIRECTION ( 'NONE',  ( 0.000000000000000000, 0.000000000000000000, 1.000000000000000000 ) ) ;
#962=CARTESIAN_POINT ( 'NONE',  ( 4.286263797015736595E-16, 1.000000000000000000, 3.500000000000000000 ) ) ;
#998=CARTESIAN_POINT ( 'NONE',  ( 0.000000000000000000, 1.000000000000000000, 0.000000000000000000 ) ) ;
#1065=EDGE_CURVE ( 'NONE', #4658, #6698, #2103, .T. ) ;
#1131=ADVANCED_FACE ( 'NONE', ( #1150, #5628 ), #10343, .T. ) ;
#1150=FACE_OUTER_BOUND ( 'NONE', #11865, .T. ) ;
#1226=UNCERTAINTY_MEASURE_WITH_UNIT (LENGTH_MEASURE( 1.000000000000000082E-05 ), #10465, 'distance_accuracy_value', 'NONE');
#1259=VECTOR ( 'NONE', #7800, 1000.000000000000000 ) ;
#1356=VERTEX_POINT ( 'NONE', #9418 ) ;
#1505=ORIENTED_EDGE ( 'NONE', *, *, #365, .F. ) ;
#1515=CIRCLE ( 'NONE', #3476, 6.000000000000002665 ) ;
#1579=CIRCLE ( 'NONE', #6519, 3.500000000000000000 ) ;
#1589=EDGE_CURVE ( 'NONE', #6397, #10866, #6683, .T. ) ;
#1657=CARTESIAN_POINT ( 'NONE',  ( 0.000000000000000000, 0.000000000000000000, 0.000000000000000000 ) ) ;
#1704=DESIGN_CONTEXT ( 'detailed design', #5805, 'design' ) ;
#1739=AXIS2_PLACEMENT_3D ( 'NONE', #6430, #872, #7587 ) ;
#1781=CARTESIAN_POINT ( 'NONE',  ( 0.000000000000000000, 0.000000000000000000, -3.500000000000000000 ) ) ;
#1983=DIRECTION ( 'NONE',  ( 0.000000000000000000, 1.000000000000000000, 0.000000000000000000 ) ) ;
#2063=CARTESIAN_POINT ( 'NONE',  ( 4.286263797015736595E-16, 0.000000000000000000, 3.500000000000000000 ) ) ;
#2103=CIRCLE ( 'NONE', #11960, 3.500000000000000000 ) ;
#2129=ORIENTED_EDGE ( 'NONE', *, *, #7120, .T. ) ;
#2196=DIRECTION ( 'NONE',  ( -0.000000000000000000, -1.000000000000000000, -0.000000000000000000 ) ) ;
#2376=FACE_OUTER_BOUND ( 'NONE', #531, .T. ) ;
#2511=( GEOMETRIC_REPRESENTATION_CONTEXT ( 3 ) GLOBAL_UNCERTAINTY_ASSIGNED_CONTEXT ( ( #1226 ) ) GLOBAL_UNIT_ASSIGNED_CONTEXT ( ( #10465, #10390, #14104 ) ) REPRESENTATION_CONTEXT ( 'NONE', 'WORKASPACE' ) );
#2822=AXIS2_PLACEMENT_3D ( 'NONE', #4457, #1983, #9170 ) ;
#2868=FACE_BOUND ( 'NONE', #8635, .T. ) ;
#2938=CARTESIAN_POINT ( 'NONE',  ( 0.000000000000000000, 1.000000000000000000, -6.000000000000002665 ) ) ;
#2956=FACE_OUTER_BOUND ( 'NONE', #12437, .T. ) ;
#3222=CIRCLE ( 'NONE', #5923, 6.000000000000002665 ) ;
#3255=CARTESIAN_POINT ( 'NONE',  ( 0.000000000000000000, 1.000000000000000000, 0.000000000000000000 ) ) ;
#3349=EDGE_CURVE ( 'NONE', #4658, #10866, #4523, .T. ) ;
#3381=CIRCLE ( 'NONE', #12020, 6.000000000000002665 ) ;
#3405=FACE_OUTER_BOUND ( 'NONE', #10616, .T. ) ;
#3476=AXIS2_PLACEMENT_3D ( 'NONE', #12364, #12136, #10049 ) ;
#3519=ORIENTED_EDGE ( 'NONE', *, *, #14418, .F. ) ;
#3532=ADVANCED_BREP_SHAPE_REPRESENTATION ( '', ( #7543, #9419 ), #2511 ) ;
#3658=DIRECTION ( 'NONE',  ( 0.000000000000000000, 1.000000000000000000, 0.000000000000000000 ) ) ;
#3666=ORIENTED_EDGE ( 'NONE', *, *, #1065, .F. ) ;
#3745=ORIENTED_EDGE ( 'NONE', *, *, #7302, .F. ) ;
#3858=ORIENTED_EDGE ( 'NONE', *, *, #10627, .F. ) ;
#3893=CLOSED_SHELL ( 'NONE', ( #5157, #6080, #1131, #5408, #6126, #5635 ) ) ;
#3980=ORIENTED_EDGE ( 'NONE', *, *, #5073, .T. ) ;
#4245=AXIS2_PLACEMENT_3D ( 'NONE', #3255, #6959, #9129 ) ;
#4367=CARTESIAN_POINT ( 'NONE',  ( 0.000000000000000000, 1.000000000000000000, 0.000000000000000000 ) ) ;
#4457=CARTESIAN_POINT ( 'NONE',  ( 0.000000000000000000, 0.000000000000000000, 0.000000000000000000 ) ) ;
#4523=LINE ( 'NONE', #962, #14836 ) ;
#4658=VERTEX_POINT ( 'NONE', #11528 ) ;
#4878=ORIENTED_EDGE ( 'NONE', *, *, #5073, .F. ) ;
#5014=ORIENTED_EDGE ( 'NONE', *, *, #1065, .T. ) ;
#5073=EDGE_CURVE ( 'NONE', #6929, #1356, #1515, .T. ) ;
#5157=ADVANCED_FACE ( 'NONE', ( #12887 ), #856, .F. ) ;
#5241=CARTESIAN_POINT ( 'NONE',  ( 0.000000000000000000, 1.000000000000000000, -3.500000000000000000 ) ) ;
#5279=VECTOR ( 'NONE', #10775, 1000.000000000000000 ) ;
#5322=LINE ( 'NONE', #12278, #7147 ) ;
#5408=ADVANCED_FACE ( 'NONE', ( #14780, #2868 ), #6486, .F. ) ;
#5538=EDGE_CURVE ( 'NONE', #13371, #14267, #3222, .T. ) ;
#5628=FACE_BOUND ( 'NONE', #15115, .T. ) ;
#5635=ADVANCED_FACE ( 'NONE', ( #2376 ), #5917, .F. ) ;
#5707=PRODUCT_DEFINITION_SHAPE ( 'NONE', 'NONE',  #10487 ) ;
#5799=CYLINDRICAL_SURFACE ( 'NONE', #4245, 6.000000000000002665 ) ;
#5805=APPLICATION_CONTEXT ( 'configuration controlled 3d designs of mechanical parts and assemblies' ) ;
#5834=PRODUCT ( 'Washer_Predeterminado', 'Washer_Predeterminado', '', ( #10492 ) ) ;
#5917=CYLINDRICAL_SURFACE ( 'NONE', #278, 3.500000000000000000 ) ;
#5923=AXIS2_PLACEMENT_3D ( 'NONE', #10643, #13508, #5996 ) ;
#5996=DIRECTION ( 'NONE',  ( 0.000000000000000000, 0.000000000000000000, 1.000000000000000000 ) ) ;
#6021=CARTESIAN_POINT ( 'NONE',  ( 0.000000000000000000, 1.000000000000000000, -6.000000000000002665 ) ) ;
#6080=ADVANCED_FACE ( 'NONE', ( #2956 ), #6739, .T. ) ;
#6126=ADVANCED_FACE ( 'NONE', ( #3405 ), #5799, .T. ) ;
#6370=DIRECTION ( 'NONE',  ( 0.000000000000000000, 1.000000000000000000, 0.000000000000000000 ) ) ;
#6397=VERTEX_POINT ( 'NONE', #1781 ) ;
#6430=CARTESIAN_POINT ( 'NONE',  ( 0.000000000000000000, 1.000000000000000000, 0.000000000000000000 ) ) ;
#6486=PLANE ( 'NONE',  #11125 ) ;
#6519=AXIS2_PLACEMENT_3D ( 'NONE', #8566, #7328, #12040 ) ;
#6521=AXIS2_PLACEMENT_3D ( 'NONE', #1657, #6370, #883 ) ;
#6569=CARTESIAN_POINT ( 'NONE',  ( 0.000000000000000000, 1.000000000000000000, 0.000000000000000000 ) ) ;
#6683=CIRCLE ( 'NONE', #7155, 3.500000000000000000 ) ;
#6698=VERTEX_POINT ( 'NONE', #5241 ) ;
#6739=CYLINDRICAL_SURFACE ( 'NONE', #1739, 6.000000000000002665 ) ;
#6755=ORIENTED_EDGE ( 'NONE', *, *, #14418, .T. ) ;
#6888=ORIENTED_EDGE ( 'NONE', *, *, #7120, .F. ) ;
#6929=VERTEX_POINT ( 'NONE', #9467 ) ;
#6959=DIRECTION ( 'NONE',  ( -0.000000000000000000, -1.000000000000000000, -0.000000000000000000 ) ) ;
#7120=EDGE_CURVE ( 'NONE', #13371, #6929, #10850, .T. ) ;
#7129=ORIENTED_EDGE ( 'NONE', *, *, #10627, .T. ) ;
#7147=VECTOR ( 'NONE', #7792, 1000.000000000000000 ) ;
#7155=AXIS2_PLACEMENT_3D ( 'NONE', #382, #14534, #13675 ) ;
#7302=EDGE_CURVE ( 'NONE', #1356, #6929, #605, .T. ) ;
#7328=DIRECTION ( 'NONE',  ( 0.000000000000000000, 1.000000000000000000, 0.000000000000000000 ) ) ;
#7543=MANIFOLD_SOLID_BREP ( 'Saliente-Extruir1', #3893 ) ;
#7587=DIRECTION ( 'NONE',  ( 0.000000000000000000, 0.000000000000000000, -1.000000000000000000 ) ) ;
#7648=AXIS2_PLACEMENT_3D ( 'NONE', #9110, #15085, #13836 ) ;
#7727=DIRECTION ( 'NONE',  ( 0.000000000000000000, 0.000000000000000000, -1.000000000000000000 ) ) ;
#7773=EDGE_LOOP ( 'NONE', ( #7129, #14642, #8087, #12949 ) ) ;
#7792=DIRECTION ( 'NONE',  ( -0.000000000000000000, -1.000000000000000000, -0.000000000000000000 ) ) ;
#7800=DIRECTION ( 'NONE',  ( -0.000000000000000000, -1.000000000000000000, -0.000000000000000000 ) ) ;
#7866=DIRECTION ( 'NONE',  ( 0.000000000000000000, -0.000000000000000000, 1.000000000000000000 ) ) ;
#7872=DIRECTION ( 'NONE',  ( 0.000000000000000000, 1.000000000000000000, 0.000000000000000000 ) ) ;
#7975=APPLICATION_CONTEXT ( 'configuration controlled 3d designs of mechanical parts and assemblies' ) ;
#8049=ORIENTED_EDGE ( 'NONE', *, *, #365, .T. ) ;
#8087=ORIENTED_EDGE ( 'NONE', *, *, #1589, .F. ) ;
#8212=SHAPE_REPRESENTATION_RELATIONSHIP ( 'NONE' , 'NONE' ,  #10790, #3532 ) ;
#8275=EDGE_LOOP ( 'NONE', ( #3745, #4878 ) ) ;
#8442=DIRECTION ( 'NONE',  ( 0.000000000000000000, 0.000000000000000000, 1.000000000000000000 ) ) ;
#8566=CARTESIAN_POINT ( 'NONE',  ( 0.000000000000000000, 1.000000000000000000, 0.000000000000000000 ) ) ;
#8635=EDGE_LOOP ( 'NONE', ( #250, #10543 ) ) ;
#8672=ORIENTED_EDGE ( 'NONE', *, *, #5538, .T. ) ;
#8884=LINE ( 'NONE', #2938, #1259 ) ;
#9110=CARTESIAN_POINT ( 'NONE',  ( 0.000000000000000000, 1.000000000000000000, 0.000000000000000000 ) ) ;
#9129=DIRECTION ( 'NONE',  ( 0.000000000000000000, 0.000000000000000000, -1.000000000000000000 ) ) ;
#9170=DIRECTION ( 'NONE',  ( 0.000000000000000000, 0.000000000000000000, 1.000000000000000000 ) ) ;
#9226=DIRECTION ( 'NONE',  ( 0.000000000000000000, 0.000000000000000000, 1.000000000000000000 ) ) ;
#9255=ORIENTED_EDGE ( 'NONE', *, *, #7302, .T. ) ;
#9418=CARTESIAN_POINT ( 'NONE',  ( 0.000000000000000000, 0.000000000000000000, -6.000000000000002665 ) ) ;
#9419=AXIS2_PLACEMENT_3D ( 'NONE', #15272, #9226, #12943 ) ;
#9467=CARTESIAN_POINT ( 'NONE',  ( 7.347880794884122694E-16, 0.000000000000000000, 6.000000000000002665 ) ) ;
#10049=DIRECTION ( 'NONE',  ( 0.000000000000000000, 0.000000000000000000, 1.000000000000000000 ) ) ;
#10343=PLANE ( 'NONE',  #7648 ) ;
#10390=( NAMED_UNIT ( * ) PLANE_ANGLE_UNIT ( ) SI_UNIT ( $, .RADIAN. ) );
#10427=DIRECTION ( 'NONE',  ( 0.000000000000000000, 0.000000000000000000, 1.000000000000000000 ) ) ;
#10465=( LENGTH_UNIT ( ) NAMED_UNIT ( * ) SI_UNIT ( .MILLI., .METRE. ) );
#10487=PRODUCT_DEFINITION ( 'UNKNOWN', '', #12090, #1704 ) ;
#10492=MECHANICAL_CONTEXT ( 'NONE', #7975, 'mechanical' ) ;
#10543=ORIENTED_EDGE ( 'NONE', *, *, #10749, .T. ) ;
#10562=ORIENTED_EDGE ( 'NONE', *, *, #13590, .T. ) ;
#10616=EDGE_LOOP ( 'NONE', ( #6888, #1505, #6755, #9255 ) ) ;
#10627=EDGE_CURVE ( 'NONE', #6698, #4658, #1579, .T. ) ;
#10635=AXIS2_PLACEMENT_3D ( 'NONE', #6569, #11353, #7727 ) ;
#10643=CARTESIAN_POINT ( 'NONE',  ( 0.000000000000000000, 1.000000000000000000, 0.000000000000000000 ) ) ;
#10714=ORIENTED_EDGE ( 'NONE', *, *, #10749, .F. ) ;
#10749=EDGE_CURVE ( 'NONE', #10866, #6397, #14439, .T. ) ;
#10775=DIRECTION ( 'NONE',  ( -0.000000000000000000, -1.000000000000000000, -0.000000000000000000 ) ) ;
#10790=SHAPE_REPRESENTATION ( 'Washer_Predeterminado', ( #9419 ), #2511 ) ;
#10850=LINE ( 'NONE', #501, #5279 ) ;
#10866=VERTEX_POINT ( 'NONE', #2063 ) ;
#11125=AXIS2_PLACEMENT_3D ( 'NONE', #13614, #12436, #7866 ) ;
#11245=DIRECTION ( 'NONE',  ( 0.000000000000000000, 0.000000000000000000, -1.000000000000000000 ) ) ;
#11353=DIRECTION ( 'NONE',  ( -0.000000000000000000, -1.000000000000000000, -0.000000000000000000 ) ) ;
#11396=DIRECTION ( 'NONE',  ( -0.000000000000000000, -1.000000000000000000, -0.000000000000000000 ) ) ;
#11528=CARTESIAN_POINT ( 'NONE',  ( 4.286263797015736595E-16, 1.000000000000000000, 3.500000000000000000 ) ) ;
#11710=ORIENTED_EDGE ( 'NONE', *, *, #3349, .F. ) ;
#11865=EDGE_LOOP ( 'NONE', ( #8049, #8672 ) ) ;
#11960=AXIS2_PLACEMENT_3D ( 'NONE', #998, #7872, #10427 ) ;
#12020=AXIS2_PLACEMENT_3D ( 'NONE', #14259, #3658, #8442 ) ;
#12040=DIRECTION ( 'NONE',  ( 0.000000000000000000, 0.000000000000000000, 1.000000000000000000 ) ) ;
#12090=PRODUCT_DEFINITION_FORMATION_WITH_SPECIFIED_SOURCE ( 'ANY', '', #5834, .NOT_KNOWN. ) ;
#12136=DIRECTION ( 'NONE',  ( 0.000000000000000000, 1.000000000000000000, 0.000000000000000000 ) ) ;
#12278=CARTESIAN_POINT ( 'NONE',  ( 0.000000000000000000, 1.000000000000000000, -3.500000000000000000 ) ) ;
#12364=CARTESIAN_POINT ( 'NONE',  ( 0.000000000000000000, 0.000000000000000000, 0.000000000000000000 ) ) ;
#12436=DIRECTION ( 'NONE',  ( 0.000000000000000000, 1.000000000000000000, 0.000000000000000000 ) ) ;
#12437=EDGE_LOOP ( 'NONE', ( #15261, #2129, #3980, #3519 ) ) ;
#12887=FACE_OUTER_BOUND ( 'NONE', #7773, .T. ) ;
#12943=DIRECTION ( 'NONE',  ( 1.000000000000000000, 0.000000000000000000, 0.000000000000000000 ) ) ;
#12949=ORIENTED_EDGE ( 'NONE', *, *, #13590, .F. ) ;
#13371=VERTEX_POINT ( 'NONE', #13394 ) ;
#13394=CARTESIAN_POINT ( 'NONE',  ( 7.347880794884122694E-16, 1.000000000000000000, 6.000000000000002665 ) ) ;
#13508=DIRECTION ( 'NONE',  ( 0.000000000000000000, 1.000000000000000000, 0.000000000000000000 ) ) ;
#13590=EDGE_CURVE ( 'NONE', #6698, #6397, #5322, .T. ) ;
#13614=CARTESIAN_POINT ( 'NONE',  ( 0.000000000000000000, 0.000000000000000000, 0.000000000000000000 ) ) ;
#13675=DIRECTION ( 'NONE',  ( 0.000000000000000000, 0.000000000000000000, 1.000000000000000000 ) ) ;
#13836=DIRECTION ( 'NONE',  ( 0.000000000000000000, -0.000000000000000000, 1.000000000000000000 ) ) ;
#14104=( NAMED_UNIT ( * ) SI_UNIT ( $, .STERADIAN. ) SOLID_ANGLE_UNIT ( ) );
#14259=CARTESIAN_POINT ( 'NONE',  ( 0.000000000000000000, 1.000000000000000000, 0.000000000000000000 ) ) ;
#14267=VERTEX_POINT ( 'NONE', #6021 ) ;
#14418=EDGE_CURVE ( 'NONE', #14267, #1356, #8884, .T. ) ;
#14439=CIRCLE ( 'NONE', #2822, 3.500000000000000000 ) ;
#14534=DIRECTION ( 'NONE',  ( 0.000000000000000000, 1.000000000000000000, 0.000000000000000000 ) ) ;
#14642=ORIENTED_EDGE ( 'NONE', *, *, #3349, .T. ) ;
#14780=FACE_OUTER_BOUND ( 'NONE', #8275, .T. ) ;
#14836=VECTOR ( 'NONE', #2196, 1000.000000000000000 ) ;
#15085=DIRECTION ( 'NONE',  ( 0.000000000000000000, 1.000000000000000000, 0.000000000000000000 ) ) ;
#15115=EDGE_LOOP ( 'NONE', ( #3858, #3666 ) ) ;
#15261=ORIENTED_EDGE ( 'NONE', *, *, #5538, .F. ) ;
#15272=CARTESIAN_POINT ( 'NONE',  ( 0.000000000000000000, 0.000000000000000000, 0.000000000000000000 ) ) ;
#15353=COLOUR_RGB('Light Gray', 0.08235294, 0.09019608, 0.10196078);
#15354=FILL_AREA_STYLE_COLOUR('',#15353);
#15355=FILL_AREA_STYLE('',(#15354));
#15356=SURFACE_STYLE_FILL_AREA(#15355);
#15357=SURFACE_SIDE_STYLE('',(#15356));
#15358=SURFACE_STYLE_USAGE(.BOTH.,#15357);
#15359=PRESENTATION_STYLE_ASSIGNMENT((#15358));
#15369=STYLED_ITEM('',(#15359),#7543);
#15370=MECHANICAL_DESIGN_GEOMETRIC_PRESENTATION_REPRESENTATION('',(#15369),#2511);
ENDSEC;
END-ISO-10303-21;
